ISO-10303-21;
HEADER;
/* Generated by software containing ST-Developer
 * from STEP Tools, Inc. (www.steptools.com) 
 */

FILE_DESCRIPTION(
/* description */ ('Over-Centre Plunger Toggle Clamp on Slotted Fixture Frame'),
/* implementation_level */ '2;1');

FILE_NAME(
/* name */ 
'M4x4 collar screw.step',
/* time_stamp */ '2026-10-28T03:23:24-07:00',
/* author */ (''),
/* organization */ (''),
/* preprocessor_version */ 'ST-DEVELOPER v20.2',
/* originating_system */ 'Autodesk Translation Framework v15.17.0.0',
/* authorisation */ '');

FILE_SCHEMA (('AUTOMOTIVE_DESIGN { 1 0 10303 214 3 1 1 }'));
ENDSEC;

DATA;
#10=MECHANICAL_DESIGN_GEOMETRIC_PRESENTATION_REPRESENTATION('',(#553),#15212);
#417=CONICAL_SURFACE('',#9512,0.185,0.785398163397449);
#461=SHAPE_REPRESENTATION_RELATIONSHIP('SRR','None',#15438,#503);
#503=ADVANCED_BREP_SHAPE_REPRESENTATION('',(#602),#15200);
#553=STYLED_ITEM('',(#15726),#602);
#602=MANIFOLD_SOLID_BREP('Body1',#8287);
#765=FACE_BOUND('',#2118,.T.);
#1015=PLANE('',#9501);
#1016=PLANE('',#9503);
#1017=PLANE('',#9504);
#1018=PLANE('',#9505);
#1019=PLANE('',#9506);
#1020=PLANE('',#9507);
#1021=PLANE('',#9508);
#1022=PLANE('',#9509);
#1023=PLANE('',#9510);
#1469=FACE_OUTER_BOUND('',#2109,.T.);
#1470=FACE_OUTER_BOUND('',#2110,.T.);
#1471=FACE_OUTER_BOUND('',#2111,.T.);
#1472=FACE_OUTER_BOUND('',#2112,.T.);
#1473=FACE_OUTER_BOUND('',#2113,.T.);
#1474=FACE_OUTER_BOUND('',#2114,.T.);
#1475=FACE_OUTER_BOUND('',#2115,.T.);
#1476=FACE_OUTER_BOUND('',#2116,.T.);
#1477=FACE_OUTER_BOUND('',#2117,.T.);
#1478=FACE_OUTER_BOUND('',#2119,.T.);
#1479=FACE_OUTER_BOUND('',#2120,.T.);
#2109=EDGE_LOOP('',(#7207));
#2110=EDGE_LOOP('',(#7208,#7209,#7210,#7211));
#2111=EDGE_LOOP('',(#7212,#7213,#7214,#7215));
#2112=EDGE_LOOP('',(#7216,#7217,#7218,#7219));
#2113=EDGE_LOOP('',(#7220,#7221,#7222,#7223));
#2114=EDGE_LOOP('',(#7224,#7225,#7226,#7227));
#2115=EDGE_LOOP('',(#7228,#7229,#7230,#7231));
#2116=EDGE_LOOP('',(#7232,#7233,#7234,#7235,#7236,#7237));
#2117=EDGE_LOOP('',(#7238));
#2118=EDGE_LOOP('',(#7239,#7240,#7241,#7242,#7243,#7244));
#2119=EDGE_LOOP('',(#7245,#7246,#7247,#7248));
#2120=EDGE_LOOP('',(#7249,#7250,#7251,#7252));
#2717=LINE('',#14569,#3347);
#2718=LINE('',#14571,#3348);
#2719=LINE('',#14573,#3349);
#2720=LINE('',#14574,#3350);
#2721=LINE('',#14577,#3351);
#2722=LINE('',#14579,#3352);
#2723=LINE('',#14580,#3353);
#2724=LINE('',#14583,#3354);
#2725=LINE('',#14585,#3355);
#2726=LINE('',#14586,#3356);
#2727=LINE('',#14589,#3357);
#2728=LINE('',#14591,#3358);
#2729=LINE('',#14592,#3359);
#2730=LINE('',#14595,#3360);
#2731=LINE('',#14597,#3361);
#2732=LINE('',#14598,#3362);
#2733=LINE('',#14600,#3363);
#2734=LINE('',#14601,#3364);
#2735=LINE('',#14609,#3365);
#2736=LINE('',#14611,#3366);
#3347=VECTOR('',#11722,1.);
#3348=VECTOR('',#11723,1.);
#3349=VECTOR('',#11724,1.);
#3350=VECTOR('',#11725,1.);
#3351=VECTOR('',#11728,1.);
#3352=VECTOR('',#11729,1.);
#3353=VECTOR('',#11730,1.);
#3354=VECTOR('',#11733,1.);
#3355=VECTOR('',#11734,1.);
#3356=VECTOR('',#11735,1.);
#3357=VECTOR('',#11738,1.);
#3358=VECTOR('',#11739,1.);
#3359=VECTOR('',#11740,1.);
#3360=VECTOR('',#11743,1.);
#3361=VECTOR('',#11744,1.);
#3362=VECTOR('',#11745,1.);
#3363=VECTOR('',#11748,1.);
#3364=VECTOR('',#11749,1.);
#3365=VECTOR('',#11760,0.185);
#3366=VECTOR('',#11763,0.2);
#3800=CIRCLE('',#9502,0.1954);
#3801=CIRCLE('',#9511,0.17);
#3802=CIRCLE('',#9513,0.1954);
#4412=VERTEX_POINT('',#14564);
#4413=VERTEX_POINT('',#14567);
#4414=VERTEX_POINT('',#14568);
#4415=VERTEX_POINT('',#14570);
#4416=VERTEX_POINT('',#14572);
#4417=VERTEX_POINT('',#14576);
#4418=VERTEX_POINT('',#14578);
#4419=VERTEX_POINT('',#14582);
#4420=VERTEX_POINT('',#14584);
#4421=VERTEX_POINT('',#14588);
#4422=VERTEX_POINT('',#14590);
#4423=VERTEX_POINT('',#14594);
#4424=VERTEX_POINT('',#14596);
#4425=VERTEX_POINT('',#14604);
#4426=VERTEX_POINT('',#14607);
#5364=EDGE_CURVE('',#4412,#4412,#3800,.T.);
#5365=EDGE_CURVE('',#4413,#4414,#2717,.T.);
#5366=EDGE_CURVE('',#4413,#4415,#2718,.T.);
#5367=EDGE_CURVE('',#4415,#4416,#2719,.T.);
#5368=EDGE_CURVE('',#4414,#4416,#2720,.T.);
#5369=EDGE_CURVE('',#4417,#4413,#2721,.T.);
#5370=EDGE_CURVE('',#4417,#4418,#2722,.T.);
#5371=EDGE_CURVE('',#4418,#4415,#2723,.T.);
#5372=EDGE_CURVE('',#4419,#4417,#2724,.T.);
#5373=EDGE_CURVE('',#4419,#4420,#2725,.T.);
#5374=EDGE_CURVE('',#4420,#4418,#2726,.T.);
#5375=EDGE_CURVE('',#4421,#4419,#2727,.T.);
#5376=EDGE_CURVE('',#4421,#4422,#2728,.T.);
#5377=EDGE_CURVE('',#4422,#4420,#2729,.T.);
#5378=EDGE_CURVE('',#4423,#4421,#2730,.T.);
#5379=EDGE_CURVE('',#4423,#4424,#2731,.T.);
#5380=EDGE_CURVE('',#4424,#4422,#2732,.T.);
#5381=EDGE_CURVE('',#4414,#4423,#2733,.T.);
#5382=EDGE_CURVE('',#4416,#4424,#2734,.T.);
#5383=EDGE_CURVE('',#4425,#4425,#3801,.T.);
#5384=EDGE_CURVE('',#4426,#4426,#3802,.T.);
#5385=EDGE_CURVE('',#4426,#4425,#2735,.T.);
#5386=EDGE_CURVE('',#4412,#4426,#2736,.T.);
#7207=ORIENTED_EDGE('',*,*,#5364,.F.);
#7208=ORIENTED_EDGE('',*,*,#5365,.F.);
#7209=ORIENTED_EDGE('',*,*,#5366,.T.);
#7210=ORIENTED_EDGE('',*,*,#5367,.T.);
#7211=ORIENTED_EDGE('',*,*,#5368,.F.);
#7212=ORIENTED_EDGE('',*,*,#5369,.F.);
#7213=ORIENTED_EDGE('',*,*,#5370,.T.);
#7214=ORIENTED_EDGE('',*,*,#5371,.T.);
#7215=ORIENTED_EDGE('',*,*,#5366,.F.);
#7216=ORIENTED_EDGE('',*,*,#5372,.F.);
#7217=ORIENTED_EDGE('',*,*,#5373,.T.);
#7218=ORIENTED_EDGE('',*,*,#5374,.T.);
#7219=ORIENTED_EDGE('',*,*,#5370,.F.);
#7220=ORIENTED_EDGE('',*,*,#5375,.F.);
#7221=ORIENTED_EDGE('',*,*,#5376,.T.);
#7222=ORIENTED_EDGE('',*,*,#5377,.T.);
#7223=ORIENTED_EDGE('',*,*,#5373,.F.);
#7224=ORIENTED_EDGE('',*,*,#5378,.F.);
#7225=ORIENTED_EDGE('',*,*,#5379,.T.);
#7226=ORIENTED_EDGE('',*,*,#5380,.T.);
#7227=ORIENTED_EDGE('',*,*,#5376,.F.);
#7228=ORIENTED_EDGE('',*,*,#5381,.F.);
#7229=ORIENTED_EDGE('',*,*,#5368,.T.);
#7230=ORIENTED_EDGE('',*,*,#5382,.T.);
#7231=ORIENTED_EDGE('',*,*,#5379,.F.);
#7232=ORIENTED_EDGE('',*,*,#5382,.F.);
#7233=ORIENTED_EDGE('',*,*,#5367,.F.);
#7234=ORIENTED_EDGE('',*,*,#5371,.F.);
#7235=ORIENTED_EDGE('',*,*,#5374,.F.);
#7236=ORIENTED_EDGE('',*,*,#5377,.F.);
#7237=ORIENTED_EDGE('',*,*,#5380,.F.);
#7238=ORIENTED_EDGE('',*,*,#5383,.F.);
#7239=ORIENTED_EDGE('',*,*,#5365,.T.);
#7240=ORIENTED_EDGE('',*,*,#5381,.T.);
#7241=ORIENTED_EDGE('',*,*,#5378,.T.);
#7242=ORIENTED_EDGE('',*,*,#5375,.T.);
#7243=ORIENTED_EDGE('',*,*,#5372,.T.);
#7244=ORIENTED_EDGE('',*,*,#5369,.T.);
#7245=ORIENTED_EDGE('',*,*,#5384,.F.);
#7246=ORIENTED_EDGE('',*,*,#5385,.T.);
#7247=ORIENTED_EDGE('',*,*,#5383,.T.);
#7248=ORIENTED_EDGE('',*,*,#5385,.F.);
#7249=ORIENTED_EDGE('',*,*,#5364,.T.);
#7250=ORIENTED_EDGE('',*,*,#5386,.T.);
#7251=ORIENTED_EDGE('',*,*,#5384,.T.);
#7252=ORIENTED_EDGE('',*,*,#5386,.F.);
#7737=CYLINDRICAL_SURFACE('',#9514,0.1954);
#8141=ADVANCED_FACE('',(#1469),#1015,.F.);
#8142=ADVANCED_FACE('',(#1470),#1016,.F.);
#8143=ADVANCED_FACE('',(#1471),#1017,.F.);
#8144=ADVANCED_FACE('',(#1472),#1018,.F.);
#8145=ADVANCED_FACE('',(#1473),#1019,.F.);
#8146=ADVANCED_FACE('',(#1474),#1020,.F.);
#8147=ADVANCED_FACE('',(#1475),#1021,.F.);
#8148=ADVANCED_FACE('',(#1476),#1022,.F.);
#8149=ADVANCED_FACE('',(#1477,#765),#1023,.T.);
#8150=ADVANCED_FACE('',(#1478),#417,.T.);
#8151=ADVANCED_FACE('',(#1479),#7737,.T.);
#8287=CLOSED_SHELL('',(#8141,#8142,#8143,#8144,#8145,#8146,#8147,#8148,
#8149,#8150,#8151));
#9500=AXIS2_PLACEMENT_3D('',#14562,#11714,#11715);
#9501=AXIS2_PLACEMENT_3D('',#14563,#11716,#11717);
#9502=AXIS2_PLACEMENT_3D('',#14565,#11718,#11719);
#9503=AXIS2_PLACEMENT_3D('',#14566,#11720,#11721);
#9504=AXIS2_PLACEMENT_3D('',#14575,#11726,#11727);
#9505=AXIS2_PLACEMENT_3D('',#14581,#11731,#11732);
#9506=AXIS2_PLACEMENT_3D('',#14587,#11736,#11737);
#9507=AXIS2_PLACEMENT_3D('',#14593,#11741,#11742);
#9508=AXIS2_PLACEMENT_3D('',#14599,#11746,#11747);
#9509=AXIS2_PLACEMENT_3D('',#14602,#11750,#11751);
#9510=AXIS2_PLACEMENT_3D('',#14603,#11752,#11753);
#9511=AXIS2_PLACEMENT_3D('',#14605,#11754,#11755);
#9512=AXIS2_PLACEMENT_3D('',#14606,#11756,#11757);
#9513=AXIS2_PLACEMENT_3D('',#14608,#11758,#11759);
#9514=AXIS2_PLACEMENT_3D('',#14610,#11761,#11762);
#11714=DIRECTION('axis',(0.,0.,1.));
#11715=DIRECTION('refdir',(1.,0.,0.));
#11716=DIRECTION('center_axis',(0.,1.,0.));
#11717=DIRECTION('ref_axis',(1.,0.,0.));
#11718=DIRECTION('center_axis',(0.,1.,0.));
#11719=DIRECTION('ref_axis',(1.,0.,0.));
#11720=DIRECTION('center_axis',(0.866025403784439,0.,-0.5));
#11721=DIRECTION('ref_axis',(0.5,0.,0.866025403784439));
#11722=DIRECTION('',(0.5,0.,0.866025403784439));
#11723=DIRECTION('',(0.,-1.,0.));
#11724=DIRECTION('',(0.5,0.,0.866025403784439));
#11725=DIRECTION('',(0.,-1.,0.));
#11726=DIRECTION('center_axis',(1.20185167898973E-16,0.,-1.));
#11727=DIRECTION('ref_axis',(1.,0.,1.20185167898973E-16));
#11728=DIRECTION('',(1.,0.,1.20185167898973E-16));
#11729=DIRECTION('',(0.,-1.,0.));
#11730=DIRECTION('',(1.,0.,1.20185167898973E-16));
#11731=DIRECTION('center_axis',(-0.866025403784439,0.,-0.5));
#11732=DIRECTION('ref_axis',(0.5,0.,-0.866025403784439));
#11733=DIRECTION('',(0.5,0.,-0.866025403784439));
#11734=DIRECTION('',(0.,-1.,0.));
#11735=DIRECTION('',(0.5,0.,-0.866025403784439));
#11736=DIRECTION('center_axis',(-0.866025403784439,0.,0.5));
#11737=DIRECTION('ref_axis',(-0.5,0.,-0.866025403784439));
#11738=DIRECTION('',(-0.5,0.,-0.866025403784439));
#11739=DIRECTION('',(0.,-1.,0.));
#11740=DIRECTION('',(-0.5,0.,-0.866025403784439));
#11741=DIRECTION('center_axis',(-2.40370335797945E-16,0.,1.));
#11742=DIRECTION('ref_axis',(-1.,0.,-2.40370335797945E-16));
#11743=DIRECTION('',(-1.,0.,-2.40370335797945E-16));
#11744=DIRECTION('',(0.,-1.,0.));
#11745=DIRECTION('',(-1.,0.,-2.40370335797945E-16));
#11746=DIRECTION('center_axis',(0.866025403784439,0.,0.5));
#11747=DIRECTION('ref_axis',(-0.5,0.,0.866025403784439));
#11748=DIRECTION('',(-0.5,0.,0.866025403784439));
#11749=DIRECTION('',(-0.5,0.,0.866025403784439));
#11750=DIRECTION('center_axis',(0.,-1.,0.));
#11751=DIRECTION('ref_axis',(0.,0.,-1.));
#11752=DIRECTION('center_axis',(0.,1.,0.));
#11753=DIRECTION('ref_axis',(0.,0.,1.));
#11754=DIRECTION('center_axis',(0.,-1.,0.));
#11755=DIRECTION('ref_axis',(1.,0.,0.));
#11756=DIRECTION('center_axis',(0.,-1.,0.));
#11757=DIRECTION('ref_axis',(1.,0.,0.));
#11758=DIRECTION('center_axis',(0.,-1.,0.));
#11759=DIRECTION('ref_axis',(1.,0.,0.));
#11760=DIRECTION('',(0.707106781186548,0.707106781186547,8.65956056235494E-17));
#11761=DIRECTION('center_axis',(0.,-1.,0.));
#11762=DIRECTION('ref_axis',(1.,0.,0.));
#11763=DIRECTION('',(0.,1.,0.));
#14562=CARTESIAN_POINT('',(0.,0.,0.));
#14563=CARTESIAN_POINT('Origin',(0.,-0.4,0.));
#14564=CARTESIAN_POINT('',(-0.1954,-0.4,2.39295984553393E-17));
#14565=CARTESIAN_POINT('Origin',(0.,-0.4,0.));
#14566=CARTESIAN_POINT('Origin',(0.0577350269189626,0.,-0.1));
#14567=CARTESIAN_POINT('',(0.0577350269189626,0.,-0.1));
#14568=CARTESIAN_POINT('',(0.115470053837925,0.,0.));
#14569=CARTESIAN_POINT('',(0.0934187836487032,0.,-0.0381939203391614));
#14570=CARTESIAN_POINT('',(0.0577350269189626,-0.2,-0.1));
#14571=CARTESIAN_POINT('',(0.0577350269189626,0.,-0.1));
#14572=CARTESIAN_POINT('',(0.115470053837925,-0.2,0.));
#14573=CARTESIAN_POINT('',(0.115470053837925,-0.2,0.));
#14574=CARTESIAN_POINT('',(0.115470053837925,0.,0.));
#14575=CARTESIAN_POINT('Origin',(-0.0577350269189626,0.,-0.1));
#14576=CARTESIAN_POINT('',(-0.0577350269189626,0.,-0.1));
#14577=CARTESIAN_POINT('',(0.0561324865405187,0.,-0.1));
#14578=CARTESIAN_POINT('',(-0.0577350269189626,-0.2,-0.1));
#14579=CARTESIAN_POINT('',(-0.0577350269189626,0.,-0.1));
#14580=CARTESIAN_POINT('',(0.0577350269189626,-0.2,-0.1));
#14581=CARTESIAN_POINT('Origin',(-0.115470053837925,0.,-1.38777878078145E-17));
#14582=CARTESIAN_POINT('',(-0.115470053837925,0.,-1.41410031829988E-17));
#14583=CARTESIAN_POINT('',(-0.0797862971081845,0.,-0.0618060796608387));
#14584=CARTESIAN_POINT('',(-0.115470053837925,-0.2,-1.38777878078145E-17));
#14585=CARTESIAN_POINT('',(-0.115470053837925,0.,-1.41410031829988E-17));
#14586=CARTESIAN_POINT('',(-0.0577350269189626,-0.2,-0.1));
#14587=CARTESIAN_POINT('Origin',(-0.0577350269189626,0.,0.1));
#14588=CARTESIAN_POINT('',(-0.0577350269189626,0.,0.1));
#14589=CARTESIAN_POINT('',(-0.0509187836487033,0.,0.111806079660839));
#14590=CARTESIAN_POINT('',(-0.0577350269189626,-0.2,0.1));
#14591=CARTESIAN_POINT('',(-0.0577350269189626,0.,0.1));
#14592=CARTESIAN_POINT('',(-0.115470053837925,-0.2,-1.41410031829988E-17));
#14593=CARTESIAN_POINT('Origin',(0.0577350269189626,0.,0.1));
#14594=CARTESIAN_POINT('',(0.0577350269189626,0.,0.1));
#14595=CARTESIAN_POINT('',(0.113867513459481,0.,0.1));
#14596=CARTESIAN_POINT('',(0.0577350269189626,-0.2,0.1));
#14597=CARTESIAN_POINT('',(0.0577350269189626,0.,0.1));
#14598=CARTESIAN_POINT('',(-0.0577350269189626,-0.2,0.1));
#14599=CARTESIAN_POINT('Origin',(0.115470053837925,0.,0.));
#14600=CARTESIAN_POINT('',(0.122286297108185,0.,-0.0118060796608386));
#14601=CARTESIAN_POINT('',(0.0577350269189626,-0.2,0.1));
#14602=CARTESIAN_POINT('Origin',(0.,-0.2,0.));
#14603=CARTESIAN_POINT('Origin',(0.17,0.,0.));
#14604=CARTESIAN_POINT('',(-0.17,-8.67361737988404E-18,-2.0818995585505E-17));
#14605=CARTESIAN_POINT('Origin',(0.,0.,0.));
#14606=CARTESIAN_POINT('Origin',(0.,-0.015,0.));
#14607=CARTESIAN_POINT('',(-0.1954,-0.0254,-2.39295984553393E-17));
#14608=CARTESIAN_POINT('Origin',(0.,-0.0254,0.));
#14609=CARTESIAN_POINT('',(-0.185,-0.015,-2.2655965784226E-17));
#14610=CARTESIAN_POINT('Origin',(0.,-0.2775,0.));
#14611=CARTESIAN_POINT('',(-0.1954,-0.2775,-2.39295984553393E-17));
#15150=UNCERTAINTY_MEASURE_WITH_UNIT(LENGTH_MEASURE(0.001),#15213,
'DISTANCE_ACCURACY_VALUE',
'Maximum model space distance between geometric entities at asserted c
onnectivities');
#15162=UNCERTAINTY_MEASURE_WITH_UNIT(LENGTH_MEASURE(0.001),#15213,
'DISTANCE_ACCURACY_VALUE',
'Maximum model space distance between geometric entities at asserted c
onnectivities');
#15200=(
GEOMETRIC_REPRESENTATION_CONTEXT(3)
GLOBAL_UNCERTAINTY_ASSIGNED_CONTEXT((#15150))
GLOBAL_UNIT_ASSIGNED_CONTEXT((#15213,#15215,#15216))
REPRESENTATION_CONTEXT('','3D')
);
#15212=(
GEOMETRIC_REPRESENTATION_CONTEXT(3)
GLOBAL_UNCERTAINTY_ASSIGNED_CONTEXT((#15162))
GLOBAL_UNIT_ASSIGNED_CONTEXT((#15213,#15215,#15216))
REPRESENTATION_CONTEXT('','3D')
);
#15213=(
LENGTH_UNIT()
NAMED_UNIT(*)
SI_UNIT(.CENTI.,.METRE.)
);
#15215=(
NAMED_UNIT(*)
PLANE_ANGLE_UNIT()
SI_UNIT($,.RADIAN.)
);
#15216=(
NAMED_UNIT(*)
SI_UNIT($,.STERADIAN.)
SOLID_ANGLE_UNIT()
);
#15254=SHAPE_DEFINITION_REPRESENTATION(#15310,#15438);
#15310=PRODUCT_DEFINITION_SHAPE('',$,#15488);
#15438=SHAPE_REPRESENTATION('',(#9500),#15200);
#15450=PRODUCT_DEFINITION_CONTEXT('part definition',#15599,'design');
#15488=PRODUCT_DEFINITION('M4x4 collar screw','M4x4 collar screw',#15537,
#15450);
#15537=PRODUCT_DEFINITION_FORMATION('',$,#15638);
#15599=APPLICATION_CONTEXT(
'Core Data for Automotive Mechanical Design Process');
#15600=PRODUCT_CONTEXT('part definition',#15599,'mechanical');
#15638=PRODUCT('M4x4 collar screw','M4x4 collar screw',
'M4x4 collar screw',(#15600));
#15720=COLOUR_RGB('Black',0.12,0.14,0.17);
#15721=FILL_AREA_STYLE_COLOUR('',#15720);
#15722=FILL_AREA_STYLE('',(#15721));
#15723=SURFACE_STYLE_FILL_AREA(#15722);
#15724=SURFACE_SIDE_STYLE('',(#15723));
#15725=SURFACE_STYLE_USAGE(.BOTH.,#15724);
#15726=PRESENTATION_STYLE_ASSIGNMENT((#15725));
ENDSEC;
END-ISO-10303-21;
